ISO-10303-21;
HEADER;
/* Generated by software containing ST-Developer
 * from STEP Tools, Inc. (www.steptools.com) 
 */

FILE_DESCRIPTION(
/* description */ ('STEP AP214'),
/* implementation_level */ '2;1');

FILE_NAME(
/* name */ 'Hex Nut 0.625-18.step',
/* time_stamp */ '2026-11-14T07:13:32-08:00',
/* author */ (''),
/* organization */ (''),
/* preprocessor_version */ 'ST-DEVELOPER v20.2',
/* originating_system */ 'Autodesk Translation Framework v15.17.0.0',
/* authorisation */ '');

FILE_SCHEMA (('AUTOMOTIVE_DESIGN { 1 0 10303 214 3 1 1 }'));
ENDSEC;

DATA;
#10=MECHANICAL_DESIGN_GEOMETRIC_PRESENTATION_REPRESENTATION('',(#1321),#32903);
#432=(
BOUNDED_CURVE()
B_SPLINE_CURVE(2,(#22941,#22942,#22943),.UNSPECIFIED.,.F.,.F.)
B_SPLINE_CURVE_WITH_KNOTS((3,3),(1.8281284674419,3.10267439666174),
 .UNSPECIFIED.)
CURVE()
GEOMETRIC_REPRESENTATION_ITEM()
RATIONAL_B_SPLINE_CURVE((1.61557985032884,1.7405453866491,1.7405453866491))
REPRESENTATION_ITEM('')
);
#433=(
BOUNDED_CURVE()
B_SPLINE_CURVE(2,(#22945,#22946,#22947),.UNSPECIFIED.,.F.,.F.)
B_SPLINE_CURVE_WITH_KNOTS((3,3),(3.10267439666174,4.3772203258816),
 .UNSPECIFIED.)
CURVE()
GEOMETRIC_REPRESENTATION_ITEM()
RATIONAL_B_SPLINE_CURVE((1.7405453866491,1.7405453866491,1.61557985032884))
REPRESENTATION_ITEM('')
);
#434=(
BOUNDED_CURVE()
B_SPLINE_CURVE(2,(#22951,#22952,#22953),.UNSPECIFIED.,.F.,.F.)
B_SPLINE_CURVE_WITH_KNOTS((3,3),(-3.10267439666174,-1.82812846744189),
 .UNSPECIFIED.)
CURVE()
GEOMETRIC_REPRESENTATION_ITEM()
RATIONAL_B_SPLINE_CURVE((1.74054538664911,1.74054538664911,1.61557985032884))
REPRESENTATION_ITEM('')
);
#435=(
BOUNDED_CURVE()
B_SPLINE_CURVE(2,(#22954,#22955,#22956),.UNSPECIFIED.,.F.,.F.)
B_SPLINE_CURVE_WITH_KNOTS((3,3),(-4.37722032588159,-3.10267439666174),
 .UNSPECIFIED.)
CURVE()
GEOMETRIC_REPRESENTATION_ITEM()
RATIONAL_B_SPLINE_CURVE((1.61557985032884,1.74054538664911,1.74054538664911))
REPRESENTATION_ITEM('')
);
#436=(
BOUNDED_CURVE()
B_SPLINE_CURVE(2,(#22959,#22960,#22961),.UNSPECIFIED.,.F.,.F.)
B_SPLINE_CURVE_WITH_KNOTS((3,3),(1.82812846744189,3.10267439666174),
 .UNSPECIFIED.)
CURVE()
GEOMETRIC_REPRESENTATION_ITEM()
RATIONAL_B_SPLINE_CURVE((1.61557985032883,1.7405453866491,1.7405453866491))
REPRESENTATION_ITEM('')
);
#437=(
BOUNDED_CURVE()
B_SPLINE_CURVE(2,(#22963,#22964,#22965),.UNSPECIFIED.,.F.,.F.)
B_SPLINE_CURVE_WITH_KNOTS((3,3),(3.10267439666174,4.37722032588159),
 .UNSPECIFIED.)
CURVE()
GEOMETRIC_REPRESENTATION_ITEM()
RATIONAL_B_SPLINE_CURVE((1.7405453866491,1.7405453866491,1.61557985032884))
REPRESENTATION_ITEM('')
);
#438=(
BOUNDED_CURVE()
B_SPLINE_CURVE(2,(#22969,#22970,#22971),.UNSPECIFIED.,.F.,.F.)
B_SPLINE_CURVE_WITH_KNOTS((3,3),(-3.10267439666174,-1.8281284674419),
 .UNSPECIFIED.)
CURVE()
GEOMETRIC_REPRESENTATION_ITEM()
RATIONAL_B_SPLINE_CURVE((1.7405453866491,1.7405453866491,1.61557985032884))
REPRESENTATION_ITEM('')
);
#439=(
BOUNDED_CURVE()
B_SPLINE_CURVE(2,(#22972,#22973,#22974),.UNSPECIFIED.,.F.,.F.)
B_SPLINE_CURVE_WITH_KNOTS((3,3),(-4.37722032588159,-3.10267439666174),
 .UNSPECIFIED.)
CURVE()
GEOMETRIC_REPRESENTATION_ITEM()
RATIONAL_B_SPLINE_CURVE((1.61557985032883,1.7405453866491,1.7405453866491))
REPRESENTATION_ITEM('')
);
#440=(
BOUNDED_CURVE()
B_SPLINE_CURVE(2,(#22978,#22979,#22980),.UNSPECIFIED.,.F.,.F.)
B_SPLINE_CURVE_WITH_KNOTS((3,3),(1.82812846744189,3.10267439666174),
 .UNSPECIFIED.)
CURVE()
GEOMETRIC_REPRESENTATION_ITEM()
RATIONAL_B_SPLINE_CURVE((1.61557985032884,1.7405453866491,1.7405453866491))
REPRESENTATION_ITEM('')
);
#441=(
BOUNDED_CURVE()
B_SPLINE_CURVE(2,(#22984,#22985,#22986),.UNSPECIFIED.,.F.,.F.)
B_SPLINE_CURVE_WITH_KNOTS((3,3),(-4.3772203258816,-3.10267439666174),
 .UNSPECIFIED.)
CURVE()
GEOMETRIC_REPRESENTATION_ITEM()
RATIONAL_B_SPLINE_CURVE((1.61557985032884,1.74054538664911,1.74054538664911))
REPRESENTATION_ITEM('')
);
#442=(
BOUNDED_CURVE()
B_SPLINE_CURVE(2,(#22987,#22988,#22989),.UNSPECIFIED.,.F.,.F.)
B_SPLINE_CURVE_WITH_KNOTS((3,3),(-3.10267439666174,-1.82812846744189),
 .UNSPECIFIED.)
CURVE()
GEOMETRIC_REPRESENTATION_ITEM()
RATIONAL_B_SPLINE_CURVE((1.74054538664911,1.74054538664911,1.61557985032884))
REPRESENTATION_ITEM('')
);
#443=(
BOUNDED_CURVE()
B_SPLINE_CURVE(2,(#22990,#22991,#22992),.UNSPECIFIED.,.F.,.F.)
B_SPLINE_CURVE_WITH_KNOTS((3,3),(3.10267439666174,4.3772203258816),
 .UNSPECIFIED.)
CURVE()
GEOMETRIC_REPRESENTATION_ITEM()
RATIONAL_B_SPLINE_CURVE((1.7405453866491,1.7405453866491,1.61557985032884))
REPRESENTATION_ITEM('')
);
#444=(
BOUNDED_CURVE()
B_SPLINE_CURVE(2,(#22995,#22996,#22997),.UNSPECIFIED.,.F.,.F.)
B_SPLINE_CURVE_WITH_KNOTS((3,3),(1.8281284674419,3.10267439666174),
 .UNSPECIFIED.)
CURVE()
GEOMETRIC_REPRESENTATION_ITEM()
RATIONAL_B_SPLINE_CURVE((1.61557985032884,1.7405453866491,1.7405453866491))
REPRESENTATION_ITEM('')
);
#445=(
BOUNDED_CURVE()
B_SPLINE_CURVE(2,(#22999,#23000,#23001),.UNSPECIFIED.,.F.,.F.)
B_SPLINE_CURVE_WITH_KNOTS((3,3),(3.10267439666174,4.3772203258816),
 .UNSPECIFIED.)
CURVE()
GEOMETRIC_REPRESENTATION_ITEM()
RATIONAL_B_SPLINE_CURVE((1.7405453866491,1.7405453866491,1.61557985032883))
REPRESENTATION_ITEM('')
);
#446=(
BOUNDED_CURVE()
B_SPLINE_CURVE(2,(#23005,#23006,#23007),.UNSPECIFIED.,.F.,.F.)
B_SPLINE_CURVE_WITH_KNOTS((3,3),(-3.10267439666174,-1.82812846744189),
 .UNSPECIFIED.)
CURVE()
GEOMETRIC_REPRESENTATION_ITEM()
RATIONAL_B_SPLINE_CURVE((1.7405453866491,1.7405453866491,1.61557985032883))
REPRESENTATION_ITEM('')
);
#447=(
BOUNDED_CURVE()
B_SPLINE_CURVE(2,(#23008,#23009,#23010),.UNSPECIFIED.,.F.,.F.)
B_SPLINE_CURVE_WITH_KNOTS((3,3),(-4.37722032588158,-3.10267439666174),
 .UNSPECIFIED.)
CURVE()
GEOMETRIC_REPRESENTATION_ITEM()
RATIONAL_B_SPLINE_CURVE((1.61557985032883,1.7405453866491,1.7405453866491))
REPRESENTATION_ITEM('')
);
#448=(
BOUNDED_CURVE()
B_SPLINE_CURVE(2,(#23013,#23014,#23015),.UNSPECIFIED.,.F.,.F.)
B_SPLINE_CURVE_WITH_KNOTS((3,3),(1.8281284674419,3.10267439666175),
 .UNSPECIFIED.)
CURVE()
GEOMETRIC_REPRESENTATION_ITEM()
RATIONAL_B_SPLINE_CURVE((1.61557985032884,1.7405453866491,1.7405453866491))
REPRESENTATION_ITEM('')
);
#449=(
BOUNDED_CURVE()
B_SPLINE_CURVE(2,(#23017,#23018,#23019),.UNSPECIFIED.,.F.,.F.)
B_SPLINE_CURVE_WITH_KNOTS((3,3),(3.10267439666175,4.37722032588158),
 .UNSPECIFIED.)
CURVE()
GEOMETRIC_REPRESENTATION_ITEM()
RATIONAL_B_SPLINE_CURVE((1.7405453866491,1.7405453866491,1.61557985032883))
REPRESENTATION_ITEM('')
);
#450=(
BOUNDED_CURVE()
B_SPLINE_CURVE(2,(#23023,#23024,#23025),.UNSPECIFIED.,.F.,.F.)
B_SPLINE_CURVE_WITH_KNOTS((3,3),(-3.10267439666174,-1.8281284674419),
 .UNSPECIFIED.)
CURVE()
GEOMETRIC_REPRESENTATION_ITEM()
RATIONAL_B_SPLINE_CURVE((1.7405453866491,1.7405453866491,1.61557985032884))
REPRESENTATION_ITEM('')
);
#451=(
BOUNDED_CURVE()
B_SPLINE_CURVE(2,(#23026,#23027,#23028),.UNSPECIFIED.,.F.,.F.)
B_SPLINE_CURVE_WITH_KNOTS((3,3),(-4.37722032588158,-3.10267439666174),
 .UNSPECIFIED.)
CURVE()
GEOMETRIC_REPRESENTATION_ITEM()
RATIONAL_B_SPLINE_CURVE((1.61557985032884,1.7405453866491,1.7405453866491))
REPRESENTATION_ITEM('')
);
#452=(
BOUNDED_CURVE()
B_SPLINE_CURVE(2,(#23031,#23032,#23033),.UNSPECIFIED.,.F.,.F.)
B_SPLINE_CURVE_WITH_KNOTS((3,3),(1.82812846744189,3.10267439666174),
 .UNSPECIFIED.)
CURVE()
GEOMETRIC_REPRESENTATION_ITEM()
RATIONAL_B_SPLINE_CURVE((1.61557985032884,1.74054538664911,1.7405453866491))
REPRESENTATION_ITEM('')
);
#453=(
BOUNDED_CURVE()
B_SPLINE_CURVE(2,(#23034,#23035,#23036),.UNSPECIFIED.,.F.,.F.)
B_SPLINE_CURVE_WITH_KNOTS((3,3),(3.10267439666174,4.37722032588159),
 .UNSPECIFIED.)
CURVE()
GEOMETRIC_REPRESENTATION_ITEM()
RATIONAL_B_SPLINE_CURVE((1.74054538664911,1.74054538664911,1.61557985032884))
REPRESENTATION_ITEM('')
);
#454=(
BOUNDED_CURVE()
B_SPLINE_CURVE(2,(#23038,#23039,#23040),.UNSPECIFIED.,.F.,.F.)
B_SPLINE_CURVE_WITH_KNOTS((3,3),(-3.10267439666174,-1.82812846744189),
 .UNSPECIFIED.)
CURVE()
GEOMETRIC_REPRESENTATION_ITEM()
RATIONAL_B_SPLINE_CURVE((1.74054538664911,1.74054538664911,1.61557985032884))
REPRESENTATION_ITEM('')
);
#455=(
BOUNDED_CURVE()
B_SPLINE_CURVE(2,(#23041,#23042,#23043),.UNSPECIFIED.,.F.,.F.)
B_SPLINE_CURVE_WITH_KNOTS((3,3),(-4.3772203258816,-3.10267439666174),
 .UNSPECIFIED.)
CURVE()
GEOMETRIC_REPRESENTATION_ITEM()
RATIONAL_B_SPLINE_CURVE((1.61557985032884,1.74054538664911,1.74054538664911))
REPRESENTATION_ITEM('')
);
#588=CONICAL_SURFACE('',#16335,7.9375,0.959931088596874);
#589=CONICAL_SURFACE('',#16338,7.282307,0.959931088596874);
#590=CONICAL_SURFACE('',#16362,11.9126,0.859709158487534);
#591=CONICAL_SURFACE('',#16363,11.9126,0.859709158487534);
#592=CONICAL_SURFACE('',#16364,11.9126,0.859709158487534);
#593=CONICAL_SURFACE('',#16365,11.9126,0.859709158487534);
#594=CONICAL_SURFACE('',#16366,11.9126,0.859709158487534);
#595=CONICAL_SURFACE('',#16367,11.9126,0.859709158487534);
#596=CONICAL_SURFACE('',#16368,11.9126,0.859709158487534);
#597=CONICAL_SURFACE('',#16369,11.9126,0.859709158487534);
#598=CONICAL_SURFACE('',#16370,11.9126,0.859709158487534);
#599=CONICAL_SURFACE('',#16371,11.9126,0.859709158487534);
#600=CONICAL_SURFACE('',#16372,11.9126,0.859709158487534);
#601=CONICAL_SURFACE('',#16373,11.9126,0.859709158487534);
#678=SHAPE_REPRESENTATION_RELATIONSHIP('SRR','None',#33020,#692);
#692=ADVANCED_BREP_SHAPE_REPRESENTATION('',(#1410),#32895);
#900=CIRCLE('',#16332,7.9375);
#901=CIRCLE('',#16333,7.9375);
#902=CIRCLE('',#16334,7.9375);
#903=CIRCLE('',#16336,7.34187);
#904=CIRCLE('',#16337,7.34187);
#905=CIRCLE('',#16339,7.34187);
#906=CIRCLE('',#16340,7.9375);
#907=CIRCLE('',#16349,11.9126);
#908=CIRCLE('',#16350,11.9126);
#909=CIRCLE('',#16351,11.9126);
#910=CIRCLE('',#16352,11.9126);
#911=CIRCLE('',#16353,11.9126);
#912=CIRCLE('',#16354,11.9126);
#913=CIRCLE('',#16356,11.9126);
#914=CIRCLE('',#16357,11.9126);
#915=CIRCLE('',#16358,11.9126);
#916=CIRCLE('',#16359,11.9126);
#917=CIRCLE('',#16360,11.9126);
#918=CIRCLE('',#16361,11.9126);
#1184=CYLINDRICAL_SURFACE('',#16331,7.9375);
#1185=CYLINDRICAL_SURFACE('',#16341,7.34187);
#1321=STYLED_ITEM('',(#33099),#1410);
#1410=MANIFOLD_SOLID_BREP('Body1',#15569);
#1597=FACE_BOUND('',#3025,.T.);
#1598=FACE_BOUND('',#3027,.T.);
#1991=FACE_OUTER_BOUND('',#3014,.T.);
#1992=FACE_OUTER_BOUND('',#3015,.T.);
#1993=FACE_OUTER_BOUND('',#3016,.T.);
#1994=FACE_OUTER_BOUND('',#3017,.T.);
#1995=FACE_OUTER_BOUND('',#3018,.T.);
#1996=FACE_OUTER_BOUND('',#3019,.T.);
#1997=FACE_OUTER_BOUND('',#3020,.T.);
#1998=FACE_OUTER_BOUND('',#3021,.T.);
#1999=FACE_OUTER_BOUND('',#3022,.T.);
#2000=FACE_OUTER_BOUND('',#3023,.T.);
#2001=FACE_OUTER_BOUND('',#3024,.T.);
#2002=FACE_OUTER_BOUND('',#3026,.T.);
#2003=FACE_OUTER_BOUND('',#3028,.T.);
#2004=FACE_OUTER_BOUND('',#3029,.T.);
#2005=FACE_OUTER_BOUND('',#3030,.T.);
#2006=FACE_OUTER_BOUND('',#3031,.T.);
#2007=FACE_OUTER_BOUND('',#3032,.T.);
#2008=FACE_OUTER_BOUND('',#3033,.T.);
#2009=FACE_OUTER_BOUND('',#3034,.T.);
#2010=FACE_OUTER_BOUND('',#3035,.T.);
#2011=FACE_OUTER_BOUND('',#3036,.T.);
#2012=FACE_OUTER_BOUND('',#3037,.T.);
#2013=FACE_OUTER_BOUND('',#3038,.T.);
#2014=FACE_OUTER_BOUND('',#3039,.T.);
#3014=EDGE_LOOP('',(#11393,#11394,#11395,#11396,#11397));
#3015=EDGE_LOOP('',(#11398,#11399,#11400,#11401,#11402,#11403));
#3016=EDGE_LOOP('',(#11404,#11405,#11406,#11407));
#3017=EDGE_LOOP('',(#11408,#11409,#11410,#11411,#11412));
#3018=EDGE_LOOP('',(#11413,#11414,#11415,#11416,#11417,#11418));
#3019=EDGE_LOOP('',(#11419,#11420,#11421,#11422,#11423,#11424));
#3020=EDGE_LOOP('',(#11425,#11426,#11427,#11428,#11429,#11430));
#3021=EDGE_LOOP('',(#11431,#11432,#11433,#11434,#11435,#11436));
#3022=EDGE_LOOP('',(#11437,#11438,#11439,#11440,#11441,#11442));
#3023=EDGE_LOOP('',(#11443,#11444,#11445,#11446,#11447,#11448));
#3024=EDGE_LOOP('',(#11449,#11450,#11451,#11452,#11453,#11454));
#3025=EDGE_LOOP('',(#11455));
#3026=EDGE_LOOP('',(#11456,#11457,#11458,#11459,#11460,#11461));
#3027=EDGE_LOOP('',(#11462));
#3028=EDGE_LOOP('',(#11463,#11464,#11465));
#3029=EDGE_LOOP('',(#11466,#11467,#11468));
#3030=EDGE_LOOP('',(#11469,#11470,#11471));
#3031=EDGE_LOOP('',(#11472,#11473,#11474));
#3032=EDGE_LOOP('',(#11475,#11476,#11477));
#3033=EDGE_LOOP('',(#11478,#11479,#11480));
#3034=EDGE_LOOP('',(#11481,#11482,#11483));
#3035=EDGE_LOOP('',(#11484,#11485,#11486));
#3036=EDGE_LOOP('',(#11487,#11488,#11489));
#3037=EDGE_LOOP('',(#11490,#11491,#11492));
#3038=EDGE_LOOP('',(#11493,#11494,#11495));
#3039=EDGE_LOOP('',(#11496,#11497,#11498));
#4168=LINE('',#22918,#5572);
#4169=LINE('',#22926,#5573);
#4170=LINE('',#22932,#5574);
#4171=LINE('',#22935,#5575);
#4172=LINE('',#22939,#5576);
#4173=LINE('',#22949,#5577);
#4174=LINE('',#22967,#5578);
#4175=LINE('',#22982,#5579);
#4176=LINE('',#23003,#5580);
#4177=LINE('',#23021,#5581);
#5572=VECTOR('',#18752,7.9375);
#5573=VECTOR('',#18761,7.9375);
#5574=VECTOR('',#18768,7.282307);
#5575=VECTOR('',#18773,7.34187);
#5576=VECTOR('',#18776,1000.);
#5577=VECTOR('',#18777,1000.);
#5578=VECTOR('',#18780,1000.);
#5579=VECTOR('',#18783,1000.);
#5580=VECTOR('',#18786,1000.);
#5581=VECTOR('',#18789,1000.);
#6971=VERTEX_POINT('',#22915);
#6972=VERTEX_POINT('',#22917);
#6973=VERTEX_POINT('',#22919);
#6974=VERTEX_POINT('',#22923);
#6975=VERTEX_POINT('',#22924);
#6976=VERTEX_POINT('',#22929);
#6977=VERTEX_POINT('',#22931);
#6978=VERTEX_POINT('',#22937);
#6979=VERTEX_POINT('',#22938);
#6980=VERTEX_POINT('',#22940);
#6981=VERTEX_POINT('',#22944);
#6982=VERTEX_POINT('',#22948);
#6983=VERTEX_POINT('',#22950);
#6984=VERTEX_POINT('',#22958);
#6985=VERTEX_POINT('',#22962);
#6986=VERTEX_POINT('',#22966);
#6987=VERTEX_POINT('',#22968);
#6988=VERTEX_POINT('',#22976);
#6989=VERTEX_POINT('',#22977);
#6990=VERTEX_POINT('',#22981);
#6991=VERTEX_POINT('',#22983);
#6992=VERTEX_POINT('',#22994);
#6993=VERTEX_POINT('',#22998);
#6994=VERTEX_POINT('',#23002);
#6995=VERTEX_POINT('',#23004);
#6996=VERTEX_POINT('',#23012);
#6997=VERTEX_POINT('',#23016);
#6998=VERTEX_POINT('',#23020);
#6999=VERTEX_POINT('',#23022);
#7000=VERTEX_POINT('',#23030);
#7001=VERTEX_POINT('',#23037);
#8580=EDGE_CURVE('',#6971,#6971,#900,.T.);
#8581=EDGE_CURVE('',#6971,#6972,#4168,.T.);
#8582=EDGE_CURVE('',#6972,#6973,#901,.T.);
#8583=EDGE_CURVE('',#6973,#6972,#902,.T.);
#8584=EDGE_CURVE('',#6974,#6975,#903,.T.);
#8585=EDGE_CURVE('',#6975,#6973,#4169,.T.);
#8586=EDGE_CURVE('',#6975,#6974,#904,.T.);
#8587=EDGE_CURVE('',#6976,#6976,#905,.T.);
#8588=EDGE_CURVE('',#6976,#6977,#4170,.T.);
#8589=EDGE_CURVE('',#6977,#6977,#906,.T.);
#8590=EDGE_CURVE('',#6974,#6976,#4171,.T.);
#8591=EDGE_CURVE('',#6978,#6979,#4172,.T.);
#8592=EDGE_CURVE('',#6979,#6980,#432,.T.);
#8593=EDGE_CURVE('',#6980,#6981,#433,.T.);
#8594=EDGE_CURVE('',#6982,#6981,#4173,.T.);
#8595=EDGE_CURVE('',#6983,#6982,#434,.T.);
#8596=EDGE_CURVE('',#6978,#6983,#435,.T.);
#8597=EDGE_CURVE('',#6981,#6984,#436,.T.);
#8598=EDGE_CURVE('',#6984,#6985,#437,.T.);
#8599=EDGE_CURVE('',#6986,#6985,#4174,.T.);
#8600=EDGE_CURVE('',#6987,#6986,#438,.T.);
#8601=EDGE_CURVE('',#6982,#6987,#439,.T.);
#8602=EDGE_CURVE('',#6988,#6989,#440,.T.);
#8603=EDGE_CURVE('',#6990,#6988,#4175,.T.);
#8604=EDGE_CURVE('',#6990,#6991,#441,.T.);
#8605=EDGE_CURVE('',#6991,#6986,#442,.T.);
#8606=EDGE_CURVE('',#6989,#6985,#443,.T.);
#8607=EDGE_CURVE('',#6988,#6992,#444,.T.);
#8608=EDGE_CURVE('',#6992,#6993,#445,.T.);
#8609=EDGE_CURVE('',#6994,#6993,#4176,.T.);
#8610=EDGE_CURVE('',#6995,#6994,#446,.T.);
#8611=EDGE_CURVE('',#6990,#6995,#447,.T.);
#8612=EDGE_CURVE('',#6993,#6996,#448,.T.);
#8613=EDGE_CURVE('',#6996,#6997,#449,.T.);
#8614=EDGE_CURVE('',#6998,#6997,#4177,.T.);
#8615=EDGE_CURVE('',#6999,#6998,#450,.T.);
#8616=EDGE_CURVE('',#6994,#6999,#451,.T.);
#8617=EDGE_CURVE('',#6997,#7000,#452,.T.);
#8618=EDGE_CURVE('',#7000,#6979,#453,.T.);
#8619=EDGE_CURVE('',#7001,#6978,#454,.T.);
#8620=EDGE_CURVE('',#6998,#7001,#455,.T.);
#8621=EDGE_CURVE('',#7000,#6980,#907,.T.);
#8622=EDGE_CURVE('',#6996,#7000,#908,.T.);
#8623=EDGE_CURVE('',#6992,#6996,#909,.T.);
#8624=EDGE_CURVE('',#6989,#6992,#910,.T.);
#8625=EDGE_CURVE('',#6989,#6984,#911,.T.);
#8626=EDGE_CURVE('',#6980,#6984,#912,.T.);
#8627=EDGE_CURVE('',#7001,#6999,#913,.T.);
#8628=EDGE_CURVE('',#6983,#7001,#914,.T.);
#8629=EDGE_CURVE('',#6987,#6983,#915,.T.);
#8630=EDGE_CURVE('',#6991,#6987,#916,.T.);
#8631=EDGE_CURVE('',#6995,#6991,#917,.T.);
#8632=EDGE_CURVE('',#6999,#6995,#918,.T.);
#11393=ORIENTED_EDGE('',*,*,#8580,.F.);
#11394=ORIENTED_EDGE('',*,*,#8581,.T.);
#11395=ORIENTED_EDGE('',*,*,#8582,.T.);
#11396=ORIENTED_EDGE('',*,*,#8583,.T.);
#11397=ORIENTED_EDGE('',*,*,#8581,.F.);
#11398=ORIENTED_EDGE('',*,*,#8584,.T.);
#11399=ORIENTED_EDGE('',*,*,#8585,.T.);
#11400=ORIENTED_EDGE('',*,*,#8582,.F.);
#11401=ORIENTED_EDGE('',*,*,#8583,.F.);
#11402=ORIENTED_EDGE('',*,*,#8585,.F.);
#11403=ORIENTED_EDGE('',*,*,#8586,.T.);
#11404=ORIENTED_EDGE('',*,*,#8587,.T.);
#11405=ORIENTED_EDGE('',*,*,#8588,.T.);
#11406=ORIENTED_EDGE('',*,*,#8589,.T.);
#11407=ORIENTED_EDGE('',*,*,#8588,.F.);
#11408=ORIENTED_EDGE('',*,*,#8584,.F.);
#11409=ORIENTED_EDGE('',*,*,#8590,.T.);
#11410=ORIENTED_EDGE('',*,*,#8587,.F.);
#11411=ORIENTED_EDGE('',*,*,#8590,.F.);
#11412=ORIENTED_EDGE('',*,*,#8586,.F.);
#11413=ORIENTED_EDGE('',*,*,#8591,.T.);
#11414=ORIENTED_EDGE('',*,*,#8592,.T.);
#11415=ORIENTED_EDGE('',*,*,#8593,.T.);
#11416=ORIENTED_EDGE('',*,*,#8594,.F.);
#11417=ORIENTED_EDGE('',*,*,#8595,.F.);
#11418=ORIENTED_EDGE('',*,*,#8596,.F.);
#11419=ORIENTED_EDGE('',*,*,#8594,.T.);
#11420=ORIENTED_EDGE('',*,*,#8597,.T.);
#11421=ORIENTED_EDGE('',*,*,#8598,.T.);
#11422=ORIENTED_EDGE('',*,*,#8599,.F.);
#11423=ORIENTED_EDGE('',*,*,#8600,.F.);
#11424=ORIENTED_EDGE('',*,*,#8601,.F.);
#11425=ORIENTED_EDGE('',*,*,#8602,.F.);
#11426=ORIENTED_EDGE('',*,*,#8603,.F.);
#11427=ORIENTED_EDGE('',*,*,#8604,.T.);
#11428=ORIENTED_EDGE('',*,*,#8605,.T.);
#11429=ORIENTED_EDGE('',*,*,#8599,.T.);
#11430=ORIENTED_EDGE('',*,*,#8606,.F.);
#11431=ORIENTED_EDGE('',*,*,#8603,.T.);
#11432=ORIENTED_EDGE('',*,*,#8607,.T.);
#11433=ORIENTED_EDGE('',*,*,#8608,.T.);
#11434=ORIENTED_EDGE('',*,*,#8609,.F.);
#11435=ORIENTED_EDGE('',*,*,#8610,.F.);
#11436=ORIENTED_EDGE('',*,*,#8611,.F.);
#11437=ORIENTED_EDGE('',*,*,#8609,.T.);
#11438=ORIENTED_EDGE('',*,*,#8612,.T.);
#11439=ORIENTED_EDGE('',*,*,#8613,.T.);
#11440=ORIENTED_EDGE('',*,*,#8614,.F.);
#11441=ORIENTED_EDGE('',*,*,#8615,.F.);
#11442=ORIENTED_EDGE('',*,*,#8616,.F.);
#11443=ORIENTED_EDGE('',*,*,#8614,.T.);
#11444=ORIENTED_EDGE('',*,*,#8617,.T.);
#11445=ORIENTED_EDGE('',*,*,#8618,.T.);
#11446=ORIENTED_EDGE('',*,*,#8591,.F.);
#11447=ORIENTED_EDGE('',*,*,#8619,.F.);
#11448=ORIENTED_EDGE('',*,*,#8620,.F.);
#11449=ORIENTED_EDGE('',*,*,#8621,.F.);
#11450=ORIENTED_EDGE('',*,*,#8622,.F.);
#11451=ORIENTED_EDGE('',*,*,#8623,.F.);
#11452=ORIENTED_EDGE('',*,*,#8624,.F.);
#11453=ORIENTED_EDGE('',*,*,#8625,.T.);
#11454=ORIENTED_EDGE('',*,*,#8626,.F.);
#11455=ORIENTED_EDGE('',*,*,#8589,.F.);
#11456=ORIENTED_EDGE('',*,*,#8627,.F.);
#11457=ORIENTED_EDGE('',*,*,#8628,.F.);
#11458=ORIENTED_EDGE('',*,*,#8629,.F.);
#11459=ORIENTED_EDGE('',*,*,#8630,.F.);
#11460=ORIENTED_EDGE('',*,*,#8631,.F.);
#11461=ORIENTED_EDGE('',*,*,#8632,.F.);
#11462=ORIENTED_EDGE('',*,*,#8580,.T.);
#11463=ORIENTED_EDGE('',*,*,#8596,.T.);
#11464=ORIENTED_EDGE('',*,*,#8628,.T.);
#11465=ORIENTED_EDGE('',*,*,#8619,.T.);
#11466=ORIENTED_EDGE('',*,*,#8595,.T.);
#11467=ORIENTED_EDGE('',*,*,#8601,.T.);
#11468=ORIENTED_EDGE('',*,*,#8629,.T.);
#11469=ORIENTED_EDGE('',*,*,#8600,.T.);
#11470=ORIENTED_EDGE('',*,*,#8605,.F.);
#11471=ORIENTED_EDGE('',*,*,#8630,.T.);
#11472=ORIENTED_EDGE('',*,*,#8611,.T.);
#11473=ORIENTED_EDGE('',*,*,#8631,.T.);
#11474=ORIENTED_EDGE('',*,*,#8604,.F.);
#11475=ORIENTED_EDGE('',*,*,#8610,.T.);
#11476=ORIENTED_EDGE('',*,*,#8616,.T.);
#11477=ORIENTED_EDGE('',*,*,#8632,.T.);
#11478=ORIENTED_EDGE('',*,*,#8615,.T.);
#11479=ORIENTED_EDGE('',*,*,#8620,.T.);
#11480=ORIENTED_EDGE('',*,*,#8627,.T.);
#11481=ORIENTED_EDGE('',*,*,#8622,.T.);
#11482=ORIENTED_EDGE('',*,*,#8617,.F.);
#11483=ORIENTED_EDGE('',*,*,#8613,.F.);
#11484=ORIENTED_EDGE('',*,*,#8623,.T.);
#11485=ORIENTED_EDGE('',*,*,#8612,.F.);
#11486=ORIENTED_EDGE('',*,*,#8608,.F.);
#11487=ORIENTED_EDGE('',*,*,#8602,.T.);
#11488=ORIENTED_EDGE('',*,*,#8624,.T.);
#11489=ORIENTED_EDGE('',*,*,#8607,.F.);
#11490=ORIENTED_EDGE('',*,*,#8625,.F.);
#11491=ORIENTED_EDGE('',*,*,#8606,.T.);
#11492=ORIENTED_EDGE('',*,*,#8598,.F.);
#11493=ORIENTED_EDGE('',*,*,#8626,.T.);
#11494=ORIENTED_EDGE('',*,*,#8597,.F.);
#11495=ORIENTED_EDGE('',*,*,#8593,.F.);
#11496=ORIENTED_EDGE('',*,*,#8618,.F.);
#11497=ORIENTED_EDGE('',*,*,#8621,.T.);
#11498=ORIENTED_EDGE('',*,*,#8592,.F.);
#14243=PLANE('',#16342);
#14244=PLANE('',#16343);
#14245=PLANE('',#16344);
#14246=PLANE('',#16345);
#14247=PLANE('',#16346);
#14248=PLANE('',#16347);
#14249=PLANE('',#16348);
#14250=PLANE('',#16355);
#14959=ADVANCED_FACE('',(#1991),#1184,.F.);
#14960=ADVANCED_FACE('',(#1992),#588,.F.);
#14961=ADVANCED_FACE('',(#1993),#589,.F.);
#14962=ADVANCED_FACE('',(#1994),#1185,.F.);
#14963=ADVANCED_FACE('',(#1995),#14243,.T.);
#14964=ADVANCED_FACE('',(#1996),#14244,.T.);
#14965=ADVANCED_FACE('',(#1997),#14245,.F.);
#14966=ADVANCED_FACE('',(#1998),#14246,.T.);
#14967=ADVANCED_FACE('',(#1999),#14247,.T.);
#14968=ADVANCED_FACE('',(#2000),#14248,.T.);
#14969=ADVANCED_FACE('',(#2001,#1597),#14249,.F.);
#14970=ADVANCED_FACE('',(#2002,#1598),#14250,.T.);
#14971=ADVANCED_FACE('',(#2003),#590,.T.);
#14972=ADVANCED_FACE('',(#2004),#591,.T.);
#14973=ADVANCED_FACE('',(#2005),#592,.T.);
#14974=ADVANCED_FACE('',(#2006),#593,.T.);
#14975=ADVANCED_FACE('',(#2007),#594,.T.);
#14976=ADVANCED_FACE('',(#2008),#595,.T.);
#14977=ADVANCED_FACE('',(#2009),#596,.T.);
#14978=ADVANCED_FACE('',(#2010),#597,.T.);
#14979=ADVANCED_FACE('',(#2011),#598,.T.);
#14980=ADVANCED_FACE('',(#2012),#599,.T.);
#14981=ADVANCED_FACE('',(#2013),#600,.T.);
#14982=ADVANCED_FACE('',(#2014),#601,.T.);
#15569=CLOSED_SHELL('',(#14959,#14960,#14961,#14962,#14963,#14964,#14965,
#14966,#14967,#14968,#14969,#14970,#14971,#14972,#14973,#14974,#14975,#14976,
#14977,#14978,#14979,#14980,#14981,#14982));
#16330=AXIS2_PLACEMENT_3D('',#22913,#18746,#18747);
#16331=AXIS2_PLACEMENT_3D('',#22914,#18748,#18749);
#16332=AXIS2_PLACEMENT_3D('',#22916,#18750,#18751);
#16333=AXIS2_PLACEMENT_3D('',#22920,#18753,#18754);
#16334=AXIS2_PLACEMENT_3D('',#22921,#18755,#18756);
#16335=AXIS2_PLACEMENT_3D('',#22922,#18757,#18758);
#16336=AXIS2_PLACEMENT_3D('',#22925,#18759,#18760);
#16337=AXIS2_PLACEMENT_3D('',#22927,#18762,#18763);
#16338=AXIS2_PLACEMENT_3D('',#22928,#18764,#18765);
#16339=AXIS2_PLACEMENT_3D('',#22930,#18766,#18767);
#16340=AXIS2_PLACEMENT_3D('',#22933,#18769,#18770);
#16341=AXIS2_PLACEMENT_3D('',#22934,#18771,#18772);
#16342=AXIS2_PLACEMENT_3D('',#22936,#18774,#18775);
#16343=AXIS2_PLACEMENT_3D('',#22957,#18778,#18779);
#16344=AXIS2_PLACEMENT_3D('',#22975,#18781,#18782);
#16345=AXIS2_PLACEMENT_3D('',#22993,#18784,#18785);
#16346=AXIS2_PLACEMENT_3D('',#23011,#18787,#18788);
#16347=AXIS2_PLACEMENT_3D('',#23029,#18790,#18791);
#16348=AXIS2_PLACEMENT_3D('',#23044,#18792,#18793);
#16349=AXIS2_PLACEMENT_3D('',#23045,#18794,#18795);
#16350=AXIS2_PLACEMENT_3D('',#23046,#18796,#18797);
#16351=AXIS2_PLACEMENT_3D('',#23047,#18798,#18799);
#16352=AXIS2_PLACEMENT_3D('',#23048,#18800,#18801);
#16353=AXIS2_PLACEMENT_3D('',#23049,#18802,#18803);
#16354=AXIS2_PLACEMENT_3D('',#23050,#18804,#18805);
#16355=AXIS2_PLACEMENT_3D('',#23051,#18806,#18807);
#16356=AXIS2_PLACEMENT_3D('',#23052,#18808,#18809);
#16357=AXIS2_PLACEMENT_3D('',#23053,#18810,#18811);
#16358=AXIS2_PLACEMENT_3D('',#23054,#18812,#18813);
#16359=AXIS2_PLACEMENT_3D('',#23055,#18814,#18815);
#16360=AXIS2_PLACEMENT_3D('',#23056,#18816,#18817);
#16361=AXIS2_PLACEMENT_3D('',#23057,#18818,#18819);
#16362=AXIS2_PLACEMENT_3D('',#23058,#18820,#18821);
#16363=AXIS2_PLACEMENT_3D('',#23059,#18822,#18823);
#16364=AXIS2_PLACEMENT_3D('',#23060,#18824,#18825);
#16365=AXIS2_PLACEMENT_3D('',#23061,#18826,#18827);
#16366=AXIS2_PLACEMENT_3D('',#23062,#18828,#18829);
#16367=AXIS2_PLACEMENT_3D('',#23063,#18830,#18831);
#16368=AXIS2_PLACEMENT_3D('',#23064,#18832,#18833);
#16369=AXIS2_PLACEMENT_3D('',#23065,#18834,#18835);
#16370=AXIS2_PLACEMENT_3D('',#23066,#18836,#18837);
#16371=AXIS2_PLACEMENT_3D('',#23067,#18838,#18839);
#16372=AXIS2_PLACEMENT_3D('',#23068,#18840,#18841);
#16373=AXIS2_PLACEMENT_3D('',#23069,#18842,#18843);
#18746=DIRECTION('axis',(0.,0.,1.));
#18747=DIRECTION('refdir',(1.,0.,0.));
#18748=DIRECTION('center_axis',(0.,0.,1.));
#18749=DIRECTION('ref_axis',(1.,0.,0.));
#18750=DIRECTION('center_axis',(0.,0.,1.));
#18751=DIRECTION('ref_axis',(-1.,0.,0.));
#18752=DIRECTION('',(0.,0.,1.));
#18753=DIRECTION('center_axis',(0.,0.,1.));
#18754=DIRECTION('ref_axis',(1.,0.,0.));
#18755=DIRECTION('center_axis',(0.,0.,1.));
#18756=DIRECTION('ref_axis',(1.,0.,0.));
#18757=DIRECTION('center_axis',(0.,0.,-1.));
#18758=DIRECTION('ref_axis',(-1.,0.,0.));
#18759=DIRECTION('center_axis',(0.,0.,1.));
#18760=DIRECTION('ref_axis',(-1.,0.,0.));
#18761=DIRECTION('',(0.819152044288988,-1.00317192905352E-16,-0.573576436351051));
#18762=DIRECTION('center_axis',(0.,0.,1.));
#18763=DIRECTION('ref_axis',(-1.,0.,0.));
#18764=DIRECTION('center_axis',(0.,0.,1.));
#18765=DIRECTION('ref_axis',(1.,0.,0.));
#18766=DIRECTION('center_axis',(0.,0.,-1.));
#18767=DIRECTION('ref_axis',(1.,0.,0.));
#18768=DIRECTION('',(-0.819152044288988,-1.00317192905352E-16,0.573576436351052));
#18769=DIRECTION('center_axis',(0.,0.,1.));
#18770=DIRECTION('ref_axis',(1.,0.,0.));
#18771=DIRECTION('center_axis',(0.,0.,1.));
#18772=DIRECTION('ref_axis',(1.,0.,0.));
#18773=DIRECTION('',(0.,0.,1.));
#18774=DIRECTION('center_axis',(-0.500000000000001,0.866025403784438,0.));
#18775=DIRECTION('ref_axis',(-0.866025403784438,-0.500000000000001,0.));
#18776=DIRECTION('',(0.,0.,1.));
#18777=DIRECTION('',(0.,0.,1.));
#18778=DIRECTION('center_axis',(0.500000000000001,0.866025403784438,0.));
#18779=DIRECTION('ref_axis',(-0.866025403784438,0.500000000000001,0.));
#18780=DIRECTION('',(0.,0.,1.));
#18781=DIRECTION('center_axis',(-1.,0.,0.));
#18782=DIRECTION('ref_axis',(0.,0.,1.));
#18783=DIRECTION('',(0.,0.,1.));
#18784=DIRECTION('center_axis',(0.500000000000001,-0.866025403784438,0.));
#18785=DIRECTION('ref_axis',(0.866025403784438,0.500000000000001,0.));
#18786=DIRECTION('',(0.,0.,1.));
#18787=DIRECTION('center_axis',(-0.500000000000001,-0.866025403784438,0.));
#18788=DIRECTION('ref_axis',(0.866025403784438,-0.500000000000001,0.));
#18789=DIRECTION('',(0.,0.,1.));
#18790=DIRECTION('center_axis',(-1.,1.26111394551748E-16,0.));
#18791=DIRECTION('ref_axis',(-1.26111394551748E-16,-1.,0.));
#18792=DIRECTION('center_axis',(0.,0.,-1.));
#18793=DIRECTION('ref_axis',(-1.,0.,0.));
#18794=DIRECTION('center_axis',(0.,0.,-1.));
#18795=DIRECTION('ref_axis',(-1.,0.,0.));
#18796=DIRECTION('center_axis',(0.,0.,-1.));
#18797=DIRECTION('ref_axis',(-1.,0.,0.));
#18798=DIRECTION('center_axis',(0.,0.,-1.));
#18799=DIRECTION('ref_axis',(-1.,0.,0.));
#18800=DIRECTION('center_axis',(0.,0.,-1.));
#18801=DIRECTION('ref_axis',(-1.,0.,0.));
#18802=DIRECTION('center_axis',(0.,0.,1.));
#18803=DIRECTION('ref_axis',(1.,0.,0.));
#18804=DIRECTION('center_axis',(0.,0.,-1.));
#18805=DIRECTION('ref_axis',(-1.,0.,0.));
#18806=DIRECTION('center_axis',(0.,0.,-1.));
#18807=DIRECTION('ref_axis',(-1.,0.,0.));
#18808=DIRECTION('center_axis',(0.,0.,1.));
#18809=DIRECTION('ref_axis',(-1.,0.,0.));
#18810=DIRECTION('center_axis',(0.,0.,1.));
#18811=DIRECTION('ref_axis',(-1.,-8.88178419700125E-16,0.));
#18812=DIRECTION('center_axis',(0.,0.,1.));
#18813=DIRECTION('ref_axis',(-1.,1.77635683940025E-15,0.));
#18814=DIRECTION('center_axis',(0.,0.,1.));
#18815=DIRECTION('ref_axis',(1.,0.,0.));
#18816=DIRECTION('center_axis',(0.,0.,1.));
#18817=DIRECTION('ref_axis',(-1.,1.77635683940025E-15,0.));
#18818=DIRECTION('center_axis',(0.,0.,1.));
#18819=DIRECTION('ref_axis',(-1.,0.,0.));
#18820=DIRECTION('center_axis',(0.,0.,1.));
#18821=DIRECTION('ref_axis',(1.,0.,0.));
#18822=DIRECTION('center_axis',(0.,0.,1.));
#18823=DIRECTION('ref_axis',(1.,0.,0.));
#18824=DIRECTION('center_axis',(0.,0.,1.));
#18825=DIRECTION('ref_axis',(1.,0.,0.));
#18826=DIRECTION('center_axis',(0.,0.,1.));
#18827=DIRECTION('ref_axis',(1.,0.,0.));
#18828=DIRECTION('center_axis',(0.,0.,1.));
#18829=DIRECTION('ref_axis',(1.,0.,0.));
#18830=DIRECTION('center_axis',(0.,0.,1.));
#18831=DIRECTION('ref_axis',(1.,0.,0.));
#18832=DIRECTION('center_axis',(0.,0.,-1.));
#18833=DIRECTION('ref_axis',(-1.,0.,0.));
#18834=DIRECTION('center_axis',(0.,0.,-1.));
#18835=DIRECTION('ref_axis',(-1.,0.,0.));
#18836=DIRECTION('center_axis',(0.,0.,-1.));
#18837=DIRECTION('ref_axis',(-1.,0.,0.));
#18838=DIRECTION('center_axis',(0.,0.,-1.));
#18839=DIRECTION('ref_axis',(-1.,0.,0.));
#18840=DIRECTION('center_axis',(0.,0.,-1.));
#18841=DIRECTION('ref_axis',(-1.,0.,0.));
#18842=DIRECTION('center_axis',(0.,0.,-1.));
#18843=DIRECTION('ref_axis',(-1.,0.,0.));
#22913=CARTESIAN_POINT('',(0.,0.,0.));
#22914=CARTESIAN_POINT('Origin',(0.,0.,-25.0375057290932));
#22915=CARTESIAN_POINT('',(-7.9375,-9.72063396823212E-16,-14.1986));
#22916=CARTESIAN_POINT('Origin',(0.,0.,-14.1986));
#22917=CARTESIAN_POINT('',(-7.9375,-9.72063396823212E-16,-14.1732));
#22918=CARTESIAN_POINT('',(-7.9375,-9.72063396823212E-16,-25.0375057290932));
#22919=CARTESIAN_POINT('',(7.9375,9.72063396823212E-16,-14.1732));
#22920=CARTESIAN_POINT('Origin',(0.,0.,-14.1732));
#22921=CARTESIAN_POINT('Origin',(0.,0.,-14.1732));
#22922=CARTESIAN_POINT('Origin',(0.,0.,-14.1732));
#22923=CARTESIAN_POINT('',(-7.34187,8.99119759525598E-16,-13.7561353840161));
#22924=CARTESIAN_POINT('',(7.34187,-8.99119759525598E-16,-13.7561353840161));
#22925=CARTESIAN_POINT('Origin',(0.,0.,-13.7561353840161));
#22926=CARTESIAN_POINT('',(7.9375,-9.72063396823212E-16,-14.1732));
#22927=CARTESIAN_POINT('Origin',(0.,0.,-13.7561353840161));
#22928=CARTESIAN_POINT('Origin',(0.,0.,-0.45877107758224));
#22929=CARTESIAN_POINT('',(-7.34187,-8.99119759525598E-16,-0.417064615983855));
#22930=CARTESIAN_POINT('Origin',(0.,0.,-0.417064615983854));
#22931=CARTESIAN_POINT('',(-7.9375,-9.72063396823212E-16,3.60822483003176E-15));
#22932=CARTESIAN_POINT('',(-7.282307,-8.91825395795836E-16,-0.45877107758224));
#22933=CARTESIAN_POINT('Origin',(0.,0.,3.46944695195361E-15));
#22934=CARTESIAN_POINT('Origin',(0.,0.,-14.1986));
#22935=CARTESIAN_POINT('',(-7.34187,-8.99119759525598E-16,-14.1986));
#22936=CARTESIAN_POINT('Origin',(4.13777825740845E-15,13.7554856334967,
-14.1986));
#22937=CARTESIAN_POINT('',(-11.9126,6.87774281674836,-12.6111));
#22938=CARTESIAN_POINT('',(-11.9126,6.87774281674833,-1.58749999999999));
#22939=CARTESIAN_POINT('',(-11.9126,6.87774281674833,-14.1986));
#22940=CARTESIAN_POINT('',(-5.95630000000001,10.3166142251225,0.));
#22941=CARTESIAN_POINT('Ctrl Pts',(-11.9125999999999,6.87774281674839,-1.58749999999993));
#22942=CARTESIAN_POINT('Ctrl Pts',(-8.72062845024497,8.72062845024502,6.66133814775094E-15));
#22943=CARTESIAN_POINT('Ctrl Pts',(-5.95630000000001,10.3166142251225,5.86830536273203E-15));
#22944=CARTESIAN_POINT('',(1.04083408558608E-14,13.7554856334967,-1.5875));
#22945=CARTESIAN_POINT('Ctrl Pts',(-5.95630000000001,10.3166142251225,5.86830536273203E-15));
#22946=CARTESIAN_POINT('Ctrl Pts',(-3.19197154975503,11.9126,4.18737605265003E-15));
#22947=CARTESIAN_POINT('Ctrl Pts',(-8.46627770245953E-14,13.7554856334966,
-1.58749999999995));
#22948=CARTESIAN_POINT('',(1.04083408558608E-14,13.7554856334967,-12.6111));
#22949=CARTESIAN_POINT('',(4.13777825740845E-15,13.7554856334967,-14.1986));
#22950=CARTESIAN_POINT('',(-5.95630000000001,10.3166142251225,-14.1986));
#22951=CARTESIAN_POINT('Ctrl Pts',(-5.9563,10.3166142251225,-14.1986));
#22952=CARTESIAN_POINT('Ctrl Pts',(-3.19197154975503,11.9126,-14.1986));
#22953=CARTESIAN_POINT('Ctrl Pts',(-9.78569760414152E-14,13.7554856334966,
-12.6111));
#22954=CARTESIAN_POINT('Ctrl Pts',(-11.9125999999999,6.87774281674841,-12.6111000000001));
#22955=CARTESIAN_POINT('Ctrl Pts',(-8.72062845024495,8.72062845024504,-14.1986));
#22956=CARTESIAN_POINT('Ctrl Pts',(-5.9563,10.3166142251225,-14.1986));
#22957=CARTESIAN_POINT('Origin',(11.9126,6.87774281674832,-14.1986));
#22958=CARTESIAN_POINT('',(5.95630000000002,10.3166142251225,0.));
#22959=CARTESIAN_POINT('Ctrl Pts',(1.20946824320851E-13,13.7554856334966,
-1.58749999999994));
#22960=CARTESIAN_POINT('Ctrl Pts',(3.19197154975505,11.9126,-5.32907051820075E-15));
#22961=CARTESIAN_POINT('Ctrl Pts',(5.95630000000001,10.3166142251225,-3.06172453707759E-15));
#22962=CARTESIAN_POINT('',(11.9126,6.87774281674836,-1.5875));
#22963=CARTESIAN_POINT('Ctrl Pts',(5.95630000000001,10.3166142251225,-3.06172453707759E-15));
#22964=CARTESIAN_POINT('Ctrl Pts',(8.72062845024497,8.72062845024502,-1.80400037842164E-15));
#22965=CARTESIAN_POINT('Ctrl Pts',(11.9125999999999,6.87774281674839,-1.58749999999993));
#22966=CARTESIAN_POINT('',(11.9126,6.87774281674836,-12.6111));
#22967=CARTESIAN_POINT('',(11.9126,6.87774281674832,-14.1986));
#22968=CARTESIAN_POINT('',(5.95630000000002,10.3166142251225,-14.1986));
#22969=CARTESIAN_POINT('Ctrl Pts',(5.95630000000004,10.3166142251225,-14.1986));
#22970=CARTESIAN_POINT('Ctrl Pts',(8.72062845024499,8.72062845024502,-14.1986));
#22971=CARTESIAN_POINT('Ctrl Pts',(11.9125999999999,6.87774281674839,-12.6111000000001));
#22972=CARTESIAN_POINT('Ctrl Pts',(1.12700449935338E-13,13.7554856334966,
-12.6111000000001));
#22973=CARTESIAN_POINT('Ctrl Pts',(3.19197154975506,11.9126,-14.1986));
#22974=CARTESIAN_POINT('Ctrl Pts',(5.95630000000004,10.3166142251225,-14.1986));
#22975=CARTESIAN_POINT('Origin',(11.9126,6.87774281674832,-14.1986));
#22976=CARTESIAN_POINT('',(11.9126,-6.87774281674836,-1.5875));
#22977=CARTESIAN_POINT('',(11.9126,0.,0.));
#22978=CARTESIAN_POINT('Ctrl Pts',(11.9126,-6.87774281674825,-1.58749999999996));
#22979=CARTESIAN_POINT('Ctrl Pts',(11.9126,-3.19197154975496,-1.55431223447522E-15));
#22980=CARTESIAN_POINT('Ctrl Pts',(11.9126,-6.12344907415516E-15,-1.81290510726578E-30));
#22981=CARTESIAN_POINT('',(11.9126,-6.87774281674836,-12.6111));
#22982=CARTESIAN_POINT('',(11.9126,-6.87774281674836,-14.1986));
#22983=CARTESIAN_POINT('',(11.9126,0.,-14.1986));
#22984=CARTESIAN_POINT('Ctrl Pts',(11.9126,-6.87774281674825,-12.6111));
#22985=CARTESIAN_POINT('Ctrl Pts',(11.9126,-3.19197154975496,-14.1986));
#22986=CARTESIAN_POINT('Ctrl Pts',(11.9126,6.12344907415516E-15,-14.1986));
#22987=CARTESIAN_POINT('Ctrl Pts',(11.9126,6.12344907415516E-15,-14.1986));
#22988=CARTESIAN_POINT('Ctrl Pts',(11.9126,3.19197154975495,-14.1986));
#22989=CARTESIAN_POINT('Ctrl Pts',(11.9126,6.87774281674823,-12.6111000000001));
#22990=CARTESIAN_POINT('Ctrl Pts',(11.9126,-6.12344907415516E-15,1.53086226853879E-15));
#22991=CARTESIAN_POINT('Ctrl Pts',(11.9126,3.19197154975495,2.72627184089894E-15));
#22992=CARTESIAN_POINT('Ctrl Pts',(11.9126,6.87774281674825,-1.58749999999996));
#22993=CARTESIAN_POINT('Origin',(-1.00154306582478E-15,-13.7554856334967,
-14.1986));
#22994=CARTESIAN_POINT('',(5.95630000000001,-10.3166142251225,0.));
#22995=CARTESIAN_POINT('Ctrl Pts',(11.9125999999999,-6.87774281674842,-1.58749999999994));
#22996=CARTESIAN_POINT('Ctrl Pts',(8.72062845024498,-8.72062845024505,-1.93178806284777E-14));
#22997=CARTESIAN_POINT('Ctrl Pts',(5.95630000000004,-10.3166142251225,-1.70946286653499E-14));
#22998=CARTESIAN_POINT('',(-5.29090660172926E-14,-13.7554856334967,-1.5875));
#22999=CARTESIAN_POINT('Ctrl Pts',(5.95630000000004,-10.3166142251225,-1.70946286653499E-14));
#23000=CARTESIAN_POINT('Ctrl Pts',(3.19197154975504,-11.9126,-1.44505874102389E-14));
#23001=CARTESIAN_POINT('Ctrl Pts',(6.92695448383054E-14,-13.7554856334967,
-1.58749999999999));
#23002=CARTESIAN_POINT('',(-5.29090660172926E-14,-13.7554856334967,-12.6111));
#23003=CARTESIAN_POINT('',(-1.00154306582478E-15,-13.7554856334967,-14.1986));
#23004=CARTESIAN_POINT('',(5.95630000000001,-10.3166142251225,-14.1986));
#23005=CARTESIAN_POINT('Ctrl Pts',(5.95630000000002,-10.3166142251225,-14.1986));
#23006=CARTESIAN_POINT('Ctrl Pts',(3.19197154975504,-11.9126,-14.1986));
#23007=CARTESIAN_POINT('Ctrl Pts',(9.5108184579578E-14,-13.7554856334967,
-12.6111));
#23008=CARTESIAN_POINT('Ctrl Pts',(11.9125999999999,-6.87774281674842,-12.6111));
#23009=CARTESIAN_POINT('Ctrl Pts',(8.72062845024498,-8.72062845024506,-14.1986));
#23010=CARTESIAN_POINT('Ctrl Pts',(5.95630000000002,-10.3166142251225,-14.1986));
#23011=CARTESIAN_POINT('Origin',(-11.9126,-6.87774281674836,-14.1986));
#23012=CARTESIAN_POINT('',(-5.95630000000001,-10.3166142251225,0.));
#23013=CARTESIAN_POINT('Ctrl Pts',(-1.53382563570533E-13,-13.7554856334966,
-1.58749999999994));
#23014=CARTESIAN_POINT('Ctrl Pts',(-3.19197154975508,-11.9126,-1.11022302462516E-14));
#23015=CARTESIAN_POINT('Ctrl Pts',(-5.95630000000005,-10.3166142251225,
-1.7349772376773E-14));
#23016=CARTESIAN_POINT('',(-11.9126,-6.87774281674836,-1.5875));
#23017=CARTESIAN_POINT('Ctrl Pts',(-5.95630000000005,-10.3166142251225,
-1.7349772376773E-14));
#23018=CARTESIAN_POINT('Ctrl Pts',(-8.720628450245,-8.72062845024504,-2.3722279033548E-14));
#23019=CARTESIAN_POINT('Ctrl Pts',(-11.9125999999999,-6.87774281674841,
-1.58749999999995));
#23020=CARTESIAN_POINT('',(-11.9126,-6.87774281674836,-12.6111));
#23021=CARTESIAN_POINT('',(-11.9126,-6.87774281674836,-14.1986));
#23022=CARTESIAN_POINT('',(-5.95630000000001,-10.3166142251225,-14.1986));
#23023=CARTESIAN_POINT('Ctrl Pts',(-5.95630000000004,-10.3166142251225,
-14.1986));
#23024=CARTESIAN_POINT('Ctrl Pts',(-8.72062845024499,-8.72062845024504,
-14.1986));
#23025=CARTESIAN_POINT('Ctrl Pts',(-11.9125999999999,-6.87774281674841,
-12.6111000000001));
#23026=CARTESIAN_POINT('Ctrl Pts',(-1.66576762587353E-13,-13.7554856334966,
-12.6111000000001));
#23027=CARTESIAN_POINT('Ctrl Pts',(-3.19197154975508,-11.9126,-14.1986));
#23028=CARTESIAN_POINT('Ctrl Pts',(-5.95630000000004,-10.3166142251225,
-14.1986));
#23029=CARTESIAN_POINT('Origin',(-11.9126,6.87774281674833,-14.1986));
#23030=CARTESIAN_POINT('',(-11.9126,1.50231459873716E-15,0.));
#23031=CARTESIAN_POINT('Ctrl Pts',(-11.9126,-6.87774281674822,-1.58749999999994));
#23032=CARTESIAN_POINT('Ctrl Pts',(-11.9126,-3.19197154975494,2.44249065417534E-15));
#23033=CARTESIAN_POINT('Ctrl Pts',(-11.9126,6.12344907415516E-15,5.10287422846262E-16));
#23034=CARTESIAN_POINT('Ctrl Pts',(-11.9126,6.12344907415516E-15,5.10287422846262E-16));
#23035=CARTESIAN_POINT('Ctrl Pts',(-11.9126,3.19197154975495,-7.93896261275937E-16));
#23036=CARTESIAN_POINT('Ctrl Pts',(-11.9126,6.87774281674822,-1.58749999999994));
#23037=CARTESIAN_POINT('',(-11.9126,1.50231459873716E-15,-14.1986));
#23038=CARTESIAN_POINT('Ctrl Pts',(-11.9126,2.04114969138505E-14,-14.1986));
#23039=CARTESIAN_POINT('Ctrl Pts',(-11.9126,3.19197154975496,-14.1986));
#23040=CARTESIAN_POINT('Ctrl Pts',(-11.9126,6.87774281674823,-12.6111000000001));
#23041=CARTESIAN_POINT('Ctrl Pts',(-11.9126,-6.87774281674826,-12.6111));
#23042=CARTESIAN_POINT('Ctrl Pts',(-11.9126,-3.19197154975495,-14.1986));
#23043=CARTESIAN_POINT('Ctrl Pts',(-11.9126,2.04114969138505E-14,-14.1986));
#23044=CARTESIAN_POINT('Origin',(5.20417042793042E-15,13.7554856334967,
0.));
#23045=CARTESIAN_POINT('Origin',(0.,0.,0.));
#23046=CARTESIAN_POINT('Origin',(0.,0.,0.));
#23047=CARTESIAN_POINT('Origin',(0.,0.,0.));
#23048=CARTESIAN_POINT('Origin',(0.,0.,0.));
#23049=CARTESIAN_POINT('Origin',(0.,0.,0.));
#23050=CARTESIAN_POINT('Origin',(0.,0.,0.));
#23051=CARTESIAN_POINT('Origin',(5.20417042793042E-15,13.7554856334967,
-14.1986));
#23052=CARTESIAN_POINT('Origin',(0.,0.,-14.1986));
#23053=CARTESIAN_POINT('Origin',(0.,0.,-14.1986));
#23054=CARTESIAN_POINT('Origin',(0.,0.,-14.1986));
#23055=CARTESIAN_POINT('Origin',(0.,0.,-14.1986));
#23056=CARTESIAN_POINT('Origin',(0.,0.,-14.1986));
#23057=CARTESIAN_POINT('Origin',(0.,0.,-14.1986));
#23058=CARTESIAN_POINT('Origin',(0.,0.,-14.1986));
#23059=CARTESIAN_POINT('Origin',(0.,0.,-14.1986));
#23060=CARTESIAN_POINT('Origin',(0.,0.,-14.1986));
#23061=CARTESIAN_POINT('Origin',(0.,0.,-14.1986));
#23062=CARTESIAN_POINT('Origin',(0.,0.,-14.1986));
#23063=CARTESIAN_POINT('Origin',(0.,0.,-14.1986));
#23064=CARTESIAN_POINT('Origin',(0.,0.,0.));
#23065=CARTESIAN_POINT('Origin',(0.,0.,0.));
#23066=CARTESIAN_POINT('Origin',(0.,0.,0.));
#23067=CARTESIAN_POINT('Origin',(0.,0.,0.));
#23068=CARTESIAN_POINT('Origin',(0.,0.,0.));
#23069=CARTESIAN_POINT('Origin',(0.,0.,0.));
#32878=UNCERTAINTY_MEASURE_WITH_UNIT(LENGTH_MEASURE(0.01),#32904,
'DISTANCE_ACCURACY_VALUE',
'Maximum model space distance between geometric entities at asserted c
onnectivities');
#32886=UNCERTAINTY_MEASURE_WITH_UNIT(LENGTH_MEASURE(0.01),#32904,
'DISTANCE_ACCURACY_VALUE',
'Maximum model space distance between geometric entities at asserted c
onnectivities');
#32895=(
GEOMETRIC_REPRESENTATION_CONTEXT(3)
GLOBAL_UNCERTAINTY_ASSIGNED_CONTEXT((#32878))
GLOBAL_UNIT_ASSIGNED_CONTEXT((#32904,#32906,#32907))
REPRESENTATION_CONTEXT('','3D')
);
#32903=(
GEOMETRIC_REPRESENTATION_CONTEXT(3)
GLOBAL_UNCERTAINTY_ASSIGNED_CONTEXT((#32886))
GLOBAL_UNIT_ASSIGNED_CONTEXT((#32904,#32906,#32907))
REPRESENTATION_CONTEXT('','3D')
);
#32904=(
LENGTH_UNIT()
NAMED_UNIT(*)
SI_UNIT(.MILLI.,.METRE.)
);
#32906=(
NAMED_UNIT(*)
PLANE_ANGLE_UNIT()
SI_UNIT($,.RADIAN.)
);
#32907=(
NAMED_UNIT(*)
SI_UNIT($,.STERADIAN.)
SOLID_ANGLE_UNIT()
);
#32916=SHAPE_DEFINITION_REPRESENTATION(#32932,#33020);
#32932=PRODUCT_DEFINITION_SHAPE('',$,#33037);
#33020=SHAPE_REPRESENTATION('',(#16330),#32895);
#33028=PRODUCT_DEFINITION_CONTEXT('part definition',#33078,'design');
#33037=PRODUCT_DEFINITION('Hex Nut 0.625-18','Hex Nut 0.625-18',#33053,
#33028);
#33053=PRODUCT_DEFINITION_FORMATION('',$,#33088);
#33078=APPLICATION_CONTEXT(
'Core Data for Automotive Mechanical Design Process');
#33079=PRODUCT_CONTEXT('part definition',#33078,'mechanical');
#33088=PRODUCT('Hex Nut 0.625-18','Hex Nut 0.625-18',$,(#33079));
#33099=PRESENTATION_STYLE_ASSIGNMENT((#33105));
#33105=SURFACE_STYLE_USAGE(.BOTH.,#33111);
#33111=SURFACE_SIDE_STYLE('',(#33117));
#33117=SURFACE_STYLE_FILL_AREA(#33123);
#33123=FILL_AREA_STYLE('Opaque(31,36,43)',(#33129));
#33129=FILL_AREA_STYLE_COLOUR('Opaque(31,36,43)',#33135);
#33135=COLOUR_RGB('Opaque(31,36,43)',0.12156862745098,0.141176470588235,
0.168627450980392);
ENDSEC;
END-ISO-10303-21;
